ISO-10303-21;
HEADER;
/* Generated by software containing ST-Developer
 * from STEP Tools, Inc. (www.steptools.com) 
 */

FILE_DESCRIPTION(
/* description */ ('Torsion-spring ratchet demonstrator'),
/* implementation_level */ '2;1');

FILE_NAME(
/* name */ 'M4x10 Cap Screw.step',
/* time_stamp */ '2026-10-29T17:29:17-07:00',
/* author */ (''),
/* organization */ (''),
/* preprocessor_version */ 'ST-DEVELOPER v20.2',
/* originating_system */ 'Autodesk Translation Framework v15.17.0.0',
/* authorisation */ '');

FILE_SCHEMA (('AUTOMOTIVE_DESIGN { 1 0 10303 214 3 1 1 }'));
ENDSEC;

DATA;
#10=MECHANICAL_DESIGN_GEOMETRIC_PRESENTATION_REPRESENTATION('',(#306),#11258);
#15=ORIENTED_CLOSED_SHELL('',*,#5178,.F.);
#17=BREP_WITH_VOIDS('Body1',#5179,(#15));
#193=CONICAL_SURFACE('',#5851,0.325,0.785398163397448);
#194=CONICAL_SURFACE('',#5855,0.335,0.785398163397448);
#195=CONICAL_SURFACE('',#5859,0.21,0.463647609000806);
#250=SHAPE_REPRESENTATION_RELATIONSHIP('SRR','None',#11377,#274);
#274=ADVANCED_BREP_SHAPE_REPRESENTATION('',(#17),#11247);
#306=STYLED_ITEM('',(#11591),#17);
#419=FACE_BOUND('',#1187,.T.);
#517=PLANE('',#5839);
#518=PLANE('',#5840);
#519=PLANE('',#5841);
#520=PLANE('',#5842);
#521=PLANE('',#5843);
#522=PLANE('',#5844);
#523=PLANE('',#5845);
#524=PLANE('',#5846);
#525=PLANE('',#5847);
#526=PLANE('',#5849);
#527=PLANE('',#5857);
#794=FACE_OUTER_BOUND('',#1173,.T.);
#795=FACE_OUTER_BOUND('',#1174,.T.);
#796=FACE_OUTER_BOUND('',#1175,.T.);
#797=FACE_OUTER_BOUND('',#1176,.T.);
#798=FACE_OUTER_BOUND('',#1177,.T.);
#799=FACE_OUTER_BOUND('',#1178,.T.);
#800=FACE_OUTER_BOUND('',#1179,.T.);
#801=FACE_OUTER_BOUND('',#1180,.T.);
#802=FACE_OUTER_BOUND('',#1181,.T.);
#803=FACE_OUTER_BOUND('',#1182,.T.);
#804=FACE_OUTER_BOUND('',#1183,.T.);
#805=FACE_OUTER_BOUND('',#1184,.T.);
#806=FACE_OUTER_BOUND('',#1185,.T.);
#807=FACE_OUTER_BOUND('',#1186,.T.);
#808=FACE_OUTER_BOUND('',#1188,.T.);
#809=FACE_OUTER_BOUND('',#1189,.T.);
#1173=EDGE_LOOP('',(#4134,#4135,#4136,#4137));
#1174=EDGE_LOOP('',(#4138,#4139,#4140,#4141));
#1175=EDGE_LOOP('',(#4142,#4143,#4144,#4145));
#1176=EDGE_LOOP('',(#4146,#4147,#4148,#4149));
#1177=EDGE_LOOP('',(#4150,#4151,#4152,#4153));
#1178=EDGE_LOOP('',(#4154,#4155,#4156,#4157));
#1179=EDGE_LOOP('',(#4158,#4159,#4160,#4161,#4162,#4163));
#1180=EDGE_LOOP('',(#4164,#4165,#4166,#4167,#4168,#4169));
#1181=EDGE_LOOP('',(#4170));
#1182=EDGE_LOOP('',(#4171));
#1183=EDGE_LOOP('',(#4172,#4173,#4174,#4175));
#1184=EDGE_LOOP('',(#4176,#4177,#4178,#4179));
#1185=EDGE_LOOP('',(#4180,#4181,#4182,#4183));
#1186=EDGE_LOOP('',(#4184));
#1187=EDGE_LOOP('',(#4185));
#1188=EDGE_LOOP('',(#4186,#4187,#4188,#4189));
#1189=EDGE_LOOP('',(#4190,#4191,#4192,#4193));
#1458=LINE('',#8864,#1841);
#1459=LINE('',#8866,#1842);
#1460=LINE('',#8868,#1843);
#1461=LINE('',#8869,#1844);
#1462=LINE('',#8872,#1845);
#1463=LINE('',#8874,#1846);
#1464=LINE('',#8875,#1847);
#1465=LINE('',#8878,#1848);
#1466=LINE('',#8880,#1849);
#1467=LINE('',#8881,#1850);
#1468=LINE('',#8884,#1851);
#1469=LINE('',#8886,#1852);
#1470=LINE('',#8887,#1853);
#1471=LINE('',#8890,#1854);
#1472=LINE('',#8892,#1855);
#1473=LINE('',#8893,#1856);
#1474=LINE('',#8895,#1857);
#1475=LINE('',#8896,#1858);
#1476=LINE('',#8908,#1859);
#1477=LINE('',#8912,#1860);
#1478=LINE('',#8916,#1861);
#1479=LINE('',#8923,#1862);
#1480=LINE('',#8925,#1863);
#1841=VECTOR('',#6973,1.);
#1842=VECTOR('',#6974,1.);
#1843=VECTOR('',#6975,1.);
#1844=VECTOR('',#6976,1.);
#1845=VECTOR('',#6979,1.);
#1846=VECTOR('',#6980,1.);
#1847=VECTOR('',#6981,1.);
#1848=VECTOR('',#6984,1.);
#1849=VECTOR('',#6985,1.);
#1850=VECTOR('',#6986,1.);
#1851=VECTOR('',#6989,1.);
#1852=VECTOR('',#6990,1.);
#1853=VECTOR('',#6991,1.);
#1854=VECTOR('',#6994,1.);
#1855=VECTOR('',#6995,1.);
#1856=VECTOR('',#6996,1.);
#1857=VECTOR('',#6999,1.);
#1858=VECTOR('',#7000,1.);
#1859=VECTOR('',#7017,0.325);
#1860=VECTOR('',#7022,0.35);
#1861=VECTOR('',#7027,0.335);
#1862=VECTOR('',#7036,0.21);
#1863=VECTOR('',#7039,0.2);
#2282=CIRCLE('',#5848,0.1954);
#2283=CIRCLE('',#5850,0.3);
#2284=CIRCLE('',#5852,0.35);
#2285=CIRCLE('',#5854,0.35);
#2286=CIRCLE('',#5856,0.32);
#2287=CIRCLE('',#5858,0.22);
#2288=CIRCLE('',#5860,0.1954);
#2574=VERTEX_POINT('',#8862);
#2575=VERTEX_POINT('',#8863);
#2576=VERTEX_POINT('',#8865);
#2577=VERTEX_POINT('',#8867);
#2578=VERTEX_POINT('',#8871);
#2579=VERTEX_POINT('',#8873);
#2580=VERTEX_POINT('',#8877);
#2581=VERTEX_POINT('',#8879);
#2582=VERTEX_POINT('',#8883);
#2583=VERTEX_POINT('',#8885);
#2584=VERTEX_POINT('',#8889);
#2585=VERTEX_POINT('',#8891);
#2586=VERTEX_POINT('',#8900);
#2587=VERTEX_POINT('',#8903);
#2588=VERTEX_POINT('',#8906);
#2589=VERTEX_POINT('',#8910);
#2590=VERTEX_POINT('',#8914);
#2591=VERTEX_POINT('',#8918);
#2592=VERTEX_POINT('',#8921);
#3127=EDGE_CURVE('',#2574,#2575,#1458,.T.);
#3128=EDGE_CURVE('',#2575,#2576,#1459,.T.);
#3129=EDGE_CURVE('',#2576,#2577,#1460,.T.);
#3130=EDGE_CURVE('',#2574,#2577,#1461,.T.);
#3131=EDGE_CURVE('',#2575,#2578,#1462,.T.);
#3132=EDGE_CURVE('',#2578,#2579,#1463,.T.);
#3133=EDGE_CURVE('',#2579,#2576,#1464,.T.);
#3134=EDGE_CURVE('',#2578,#2580,#1465,.T.);
#3135=EDGE_CURVE('',#2580,#2581,#1466,.T.);
#3136=EDGE_CURVE('',#2581,#2579,#1467,.T.);
#3137=EDGE_CURVE('',#2580,#2582,#1468,.T.);
#3138=EDGE_CURVE('',#2582,#2583,#1469,.T.);
#3139=EDGE_CURVE('',#2583,#2581,#1470,.T.);
#3140=EDGE_CURVE('',#2582,#2584,#1471,.T.);
#3141=EDGE_CURVE('',#2584,#2585,#1472,.T.);
#3142=EDGE_CURVE('',#2585,#2583,#1473,.T.);
#3143=EDGE_CURVE('',#2584,#2574,#1474,.T.);
#3144=EDGE_CURVE('',#2577,#2585,#1475,.T.);
#3145=EDGE_CURVE('',#2586,#2586,#2282,.T.);
#3146=EDGE_CURVE('',#2587,#2587,#2283,.T.);
#3147=EDGE_CURVE('',#2588,#2588,#2284,.T.);
#3148=EDGE_CURVE('',#2588,#2587,#1476,.T.);
#3149=EDGE_CURVE('',#2589,#2589,#2285,.T.);
#3150=EDGE_CURVE('',#2589,#2588,#1477,.T.);
#3151=EDGE_CURVE('',#2590,#2590,#2286,.T.);
#3152=EDGE_CURVE('',#2590,#2589,#1478,.T.);
#3153=EDGE_CURVE('',#2591,#2591,#2287,.T.);
#3154=EDGE_CURVE('',#2592,#2592,#2288,.F.);
#3155=EDGE_CURVE('',#2592,#2591,#1479,.T.);
#3156=EDGE_CURVE('',#2586,#2592,#1480,.T.);
#4134=ORIENTED_EDGE('',*,*,#3127,.T.);
#4135=ORIENTED_EDGE('',*,*,#3128,.T.);
#4136=ORIENTED_EDGE('',*,*,#3129,.T.);
#4137=ORIENTED_EDGE('',*,*,#3130,.F.);
#4138=ORIENTED_EDGE('',*,*,#3131,.T.);
#4139=ORIENTED_EDGE('',*,*,#3132,.T.);
#4140=ORIENTED_EDGE('',*,*,#3133,.T.);
#4141=ORIENTED_EDGE('',*,*,#3128,.F.);
#4142=ORIENTED_EDGE('',*,*,#3134,.T.);
#4143=ORIENTED_EDGE('',*,*,#3135,.T.);
#4144=ORIENTED_EDGE('',*,*,#3136,.T.);
#4145=ORIENTED_EDGE('',*,*,#3132,.F.);
#4146=ORIENTED_EDGE('',*,*,#3137,.T.);
#4147=ORIENTED_EDGE('',*,*,#3138,.T.);
#4148=ORIENTED_EDGE('',*,*,#3139,.T.);
#4149=ORIENTED_EDGE('',*,*,#3135,.F.);
#4150=ORIENTED_EDGE('',*,*,#3140,.T.);
#4151=ORIENTED_EDGE('',*,*,#3141,.T.);
#4152=ORIENTED_EDGE('',*,*,#3142,.T.);
#4153=ORIENTED_EDGE('',*,*,#3138,.F.);
#4154=ORIENTED_EDGE('',*,*,#3143,.T.);
#4155=ORIENTED_EDGE('',*,*,#3130,.T.);
#4156=ORIENTED_EDGE('',*,*,#3144,.T.);
#4157=ORIENTED_EDGE('',*,*,#3141,.F.);
#4158=ORIENTED_EDGE('',*,*,#3143,.F.);
#4159=ORIENTED_EDGE('',*,*,#3140,.F.);
#4160=ORIENTED_EDGE('',*,*,#3137,.F.);
#4161=ORIENTED_EDGE('',*,*,#3134,.F.);
#4162=ORIENTED_EDGE('',*,*,#3131,.F.);
#4163=ORIENTED_EDGE('',*,*,#3127,.F.);
#4164=ORIENTED_EDGE('',*,*,#3144,.F.);
#4165=ORIENTED_EDGE('',*,*,#3129,.F.);
#4166=ORIENTED_EDGE('',*,*,#3133,.F.);
#4167=ORIENTED_EDGE('',*,*,#3136,.F.);
#4168=ORIENTED_EDGE('',*,*,#3139,.F.);
#4169=ORIENTED_EDGE('',*,*,#3142,.F.);
#4170=ORIENTED_EDGE('',*,*,#3145,.F.);
#4171=ORIENTED_EDGE('',*,*,#3146,.F.);
#4172=ORIENTED_EDGE('',*,*,#3147,.F.);
#4173=ORIENTED_EDGE('',*,*,#3148,.T.);
#4174=ORIENTED_EDGE('',*,*,#3146,.T.);
#4175=ORIENTED_EDGE('',*,*,#3148,.F.);
#4176=ORIENTED_EDGE('',*,*,#3149,.F.);
#4177=ORIENTED_EDGE('',*,*,#3150,.T.);
#4178=ORIENTED_EDGE('',*,*,#3147,.T.);
#4179=ORIENTED_EDGE('',*,*,#3150,.F.);
#4180=ORIENTED_EDGE('',*,*,#3151,.F.);
#4181=ORIENTED_EDGE('',*,*,#3152,.T.);
#4182=ORIENTED_EDGE('',*,*,#3149,.T.);
#4183=ORIENTED_EDGE('',*,*,#3152,.F.);
#4184=ORIENTED_EDGE('',*,*,#3151,.T.);
#4185=ORIENTED_EDGE('',*,*,#3153,.F.);
#4186=ORIENTED_EDGE('',*,*,#3154,.F.);
#4187=ORIENTED_EDGE('',*,*,#3155,.T.);
#4188=ORIENTED_EDGE('',*,*,#3153,.T.);
#4189=ORIENTED_EDGE('',*,*,#3155,.F.);
#4190=ORIENTED_EDGE('',*,*,#3145,.T.);
#4191=ORIENTED_EDGE('',*,*,#3156,.T.);
#4192=ORIENTED_EDGE('',*,*,#3154,.T.);
#4193=ORIENTED_EDGE('',*,*,#3156,.F.);
#4830=CYLINDRICAL_SURFACE('',#5853,0.35);
#4831=CYLINDRICAL_SURFACE('',#5861,0.1954);
#5020=ADVANCED_FACE('',(#794),#517,.F.);
#5021=ADVANCED_FACE('',(#795),#518,.F.);
#5022=ADVANCED_FACE('',(#796),#519,.F.);
#5023=ADVANCED_FACE('',(#797),#520,.F.);
#5024=ADVANCED_FACE('',(#798),#521,.F.);
#5025=ADVANCED_FACE('',(#799),#522,.F.);
#5026=ADVANCED_FACE('',(#800),#523,.F.);
#5027=ADVANCED_FACE('',(#801),#524,.F.);
#5028=ADVANCED_FACE('',(#802),#525,.F.);
#5029=ADVANCED_FACE('',(#803),#526,.T.);
#5030=ADVANCED_FACE('',(#804),#193,.T.);
#5031=ADVANCED_FACE('',(#805),#4830,.T.);
#5032=ADVANCED_FACE('',(#806),#194,.T.);
#5033=ADVANCED_FACE('',(#807,#419),#527,.T.);
#5034=ADVANCED_FACE('',(#808),#195,.T.);
#5035=ADVANCED_FACE('',(#809),#4831,.T.);
#5178=CLOSED_SHELL('',(#5020,#5021,#5022,#5023,#5024,#5025,#5026,#5027));
#5179=CLOSED_SHELL('',(#5028,#5029,#5030,#5031,#5032,#5033,#5034,#5035));
#5838=AXIS2_PLACEMENT_3D('',#8860,#6969,#6970);
#5839=AXIS2_PLACEMENT_3D('',#8861,#6971,#6972);
#5840=AXIS2_PLACEMENT_3D('',#8870,#6977,#6978);
#5841=AXIS2_PLACEMENT_3D('',#8876,#6982,#6983);
#5842=AXIS2_PLACEMENT_3D('',#8882,#6987,#6988);
#5843=AXIS2_PLACEMENT_3D('',#8888,#6992,#6993);
#5844=AXIS2_PLACEMENT_3D('',#8894,#6997,#6998);
#5845=AXIS2_PLACEMENT_3D('',#8897,#7001,#7002);
#5846=AXIS2_PLACEMENT_3D('',#8898,#7003,#7004);
#5847=AXIS2_PLACEMENT_3D('',#8899,#7005,#7006);
#5848=AXIS2_PLACEMENT_3D('',#8901,#7007,#7008);
#5849=AXIS2_PLACEMENT_3D('',#8902,#7009,#7010);
#5850=AXIS2_PLACEMENT_3D('',#8904,#7011,#7012);
#5851=AXIS2_PLACEMENT_3D('',#8905,#7013,#7014);
#5852=AXIS2_PLACEMENT_3D('',#8907,#7015,#7016);
#5853=AXIS2_PLACEMENT_3D('',#8909,#7018,#7019);
#5854=AXIS2_PLACEMENT_3D('',#8911,#7020,#7021);
#5855=AXIS2_PLACEMENT_3D('',#8913,#7023,#7024);
#5856=AXIS2_PLACEMENT_3D('',#8915,#7025,#7026);
#5857=AXIS2_PLACEMENT_3D('',#8917,#7028,#7029);
#5858=AXIS2_PLACEMENT_3D('',#8919,#7030,#7031);
#5859=AXIS2_PLACEMENT_3D('',#8920,#7032,#7033);
#5860=AXIS2_PLACEMENT_3D('',#8922,#7034,#7035);
#5861=AXIS2_PLACEMENT_3D('',#8924,#7037,#7038);
#6969=DIRECTION('axis',(0.,0.,1.));
#6970=DIRECTION('refdir',(1.,0.,0.));
#6971=DIRECTION('center_axis',(0.866025403784439,0.,-0.5));
#6972=DIRECTION('ref_axis',(0.5,0.,0.866025403784439));
#6973=DIRECTION('',(-0.5,0.,-0.866025403784439));
#6974=DIRECTION('',(0.,-1.,0.));
#6975=DIRECTION('',(0.5,0.,0.866025403784439));
#6976=DIRECTION('',(0.,-1.,0.));
#6977=DIRECTION('center_axis',(1.60246890531964E-16,0.,-1.));
#6978=DIRECTION('ref_axis',(1.,0.,1.60246890531964E-16));
#6979=DIRECTION('',(-1.,0.,-1.60246890531964E-16));
#6980=DIRECTION('',(0.,-1.,0.));
#6981=DIRECTION('',(1.,0.,1.60246890531964E-16));
#6982=DIRECTION('center_axis',(-0.866025403784439,0.,-0.5));
#6983=DIRECTION('ref_axis',(0.5,0.,-0.866025403784439));
#6984=DIRECTION('',(-0.5,0.,0.866025403784439));
#6985=DIRECTION('',(0.,-1.,0.));
#6986=DIRECTION('',(0.5,0.,-0.866025403784439));
#6987=DIRECTION('center_axis',(-0.866025403784439,0.,0.5));
#6988=DIRECTION('ref_axis',(-0.5,0.,-0.866025403784439));
#6989=DIRECTION('',(0.5,0.,0.866025403784439));
#6990=DIRECTION('',(0.,-1.,0.));
#6991=DIRECTION('',(-0.5,0.,-0.866025403784439));
#6992=DIRECTION('center_axis',(-1.60246890531964E-16,0.,1.));
#6993=DIRECTION('ref_axis',(-1.,0.,-1.60246890531964E-16));
#6994=DIRECTION('',(1.,0.,1.60246890531964E-16));
#6995=DIRECTION('',(0.,-1.,0.));
#6996=DIRECTION('',(-1.,0.,-1.60246890531964E-16));
#6997=DIRECTION('center_axis',(0.866025403784439,0.,0.5));
#6998=DIRECTION('ref_axis',(-0.5,0.,0.866025403784439));
#6999=DIRECTION('',(0.5,0.,-0.866025403784439));
#7000=DIRECTION('',(-0.5,0.,0.866025403784439));
#7001=DIRECTION('center_axis',(0.,1.,0.));
#7002=DIRECTION('ref_axis',(1.,0.,0.));
#7003=DIRECTION('center_axis',(0.,-1.,0.));
#7004=DIRECTION('ref_axis',(0.,0.,-1.));
#7005=DIRECTION('center_axis',(0.,1.,0.));
#7006=DIRECTION('ref_axis',(1.,0.,0.));
#7007=DIRECTION('center_axis',(0.,1.,0.));
#7008=DIRECTION('ref_axis',(1.,0.,0.));
#7009=DIRECTION('center_axis',(0.,1.,0.));
#7010=DIRECTION('ref_axis',(0.,0.,1.));
#7011=DIRECTION('center_axis',(0.,-1.,0.));
#7012=DIRECTION('ref_axis',(1.,0.,0.));
#7013=DIRECTION('center_axis',(0.,-1.,0.));
#7014=DIRECTION('ref_axis',(1.,0.,0.));
#7015=DIRECTION('center_axis',(0.,-1.,0.));
#7016=DIRECTION('ref_axis',(1.,0.,0.));
#7017=DIRECTION('',(0.707106781186547,0.707106781186548,8.65956056235493E-17));
#7018=DIRECTION('center_axis',(0.,-1.,0.));
#7019=DIRECTION('ref_axis',(1.,0.,0.));
#7020=DIRECTION('center_axis',(0.,-1.,0.));
#7021=DIRECTION('ref_axis',(1.,0.,0.));
#7022=DIRECTION('',(0.,1.,0.));
#7023=DIRECTION('center_axis',(0.,1.,0.));
#7024=DIRECTION('ref_axis',(1.,0.,0.));
#7025=DIRECTION('center_axis',(0.,-1.,0.));
#7026=DIRECTION('ref_axis',(1.,0.,0.));
#7027=DIRECTION('',(-0.707106781186547,0.707106781186548,-8.65956056235493E-17));
#7028=DIRECTION('center_axis',(0.,-1.,0.));
#7029=DIRECTION('ref_axis',(0.,0.,-1.));
#7030=DIRECTION('center_axis',(0.,-1.,0.));
#7031=DIRECTION('ref_axis',(1.,0.,0.));
#7032=DIRECTION('center_axis',(0.,1.,0.));
#7033=DIRECTION('ref_axis',(1.,0.,0.));
#7034=DIRECTION('center_axis',(0.,1.,0.));
#7035=DIRECTION('ref_axis',(1.,0.,0.));
#7036=DIRECTION('',(-0.447213595499958,0.894427190999916,-5.47678698264203E-17));
#7037=DIRECTION('center_axis',(0.,-1.,0.));
#7038=DIRECTION('ref_axis',(1.,0.,0.));
#7039=DIRECTION('',(0.,1.,0.));
#8860=CARTESIAN_POINT('',(0.,0.,0.));
#8861=CARTESIAN_POINT('Origin',(0.0866025403784439,-0.4,-0.15));
#8862=CARTESIAN_POINT('',(0.173205080756888,-0.4,0.));
#8863=CARTESIAN_POINT('',(0.0866025403784439,-0.4,-0.15));
#8864=CARTESIAN_POINT('',(0.173205080756888,-0.4,0.));
#8865=CARTESIAN_POINT('',(0.0866025403784439,-0.64,-0.15));
#8866=CARTESIAN_POINT('',(0.0866025403784439,-0.4,-0.15));
#8867=CARTESIAN_POINT('',(0.173205080756888,-0.64,0.));
#8868=CARTESIAN_POINT('',(0.173205080756888,-0.64,0.));
#8869=CARTESIAN_POINT('',(0.173205080756888,-0.4,0.));
#8870=CARTESIAN_POINT('Origin',(-0.0866025403784438,-0.4,-0.15));
#8871=CARTESIAN_POINT('',(-0.0866025403784438,-0.4,-0.15));
#8872=CARTESIAN_POINT('',(0.0866025403784439,-0.4,-0.15));
#8873=CARTESIAN_POINT('',(-0.0866025403784438,-0.64,-0.15));
#8874=CARTESIAN_POINT('',(-0.0866025403784438,-0.4,-0.15));
#8875=CARTESIAN_POINT('',(0.0866025403784439,-0.64,-0.15));
#8876=CARTESIAN_POINT('Origin',(-0.173205080756888,-0.4,-2.77555756156289E-17));
#8877=CARTESIAN_POINT('',(-0.173205080756888,-0.4,-2.12115047744981E-17));
#8878=CARTESIAN_POINT('',(-0.0866025403784438,-0.4,-0.15));
#8879=CARTESIAN_POINT('',(-0.173205080756888,-0.64,-2.77555756156289E-17));
#8880=CARTESIAN_POINT('',(-0.173205080756888,-0.4,-2.12115047744981E-17));
#8881=CARTESIAN_POINT('',(-0.0866025403784438,-0.64,-0.15));
#8882=CARTESIAN_POINT('Origin',(-0.0866025403784439,-0.4,0.15));
#8883=CARTESIAN_POINT('',(-0.0866025403784439,-0.4,0.15));
#8884=CARTESIAN_POINT('',(-0.173205080756888,-0.4,-2.12115047744981E-17));
#8885=CARTESIAN_POINT('',(-0.0866025403784439,-0.64,0.15));
#8886=CARTESIAN_POINT('',(-0.0866025403784439,-0.4,0.15));
#8887=CARTESIAN_POINT('',(-0.173205080756888,-0.64,-2.12115047744981E-17));
#8888=CARTESIAN_POINT('Origin',(0.0866025403784439,-0.4,0.15));
#8889=CARTESIAN_POINT('',(0.0866025403784439,-0.4,0.15));
#8890=CARTESIAN_POINT('',(-0.0866025403784439,-0.4,0.15));
#8891=CARTESIAN_POINT('',(0.0866025403784439,-0.64,0.15));
#8892=CARTESIAN_POINT('',(0.0866025403784439,-0.4,0.15));
#8893=CARTESIAN_POINT('',(-0.0866025403784439,-0.64,0.15));
#8894=CARTESIAN_POINT('Origin',(0.173205080756888,-0.4,0.));
#8895=CARTESIAN_POINT('',(0.0866025403784439,-0.4,0.15));
#8896=CARTESIAN_POINT('',(0.0866025403784439,-0.64,0.15));
#8897=CARTESIAN_POINT('Origin',(0.,-0.4,-2.77555756156289E-17));
#8898=CARTESIAN_POINT('Origin',(0.,-0.64,-2.77555756156289E-17));
#8899=CARTESIAN_POINT('Origin',(0.,-1.,0.));
#8900=CARTESIAN_POINT('',(-0.1954,-1.,2.39295984553393E-17));
#8901=CARTESIAN_POINT('Origin',(0.,-1.,0.));
#8902=CARTESIAN_POINT('Origin',(0.3,0.4,0.));
#8903=CARTESIAN_POINT('',(-0.3,0.4,-3.67394039744206E-17));
#8904=CARTESIAN_POINT('Origin',(0.,0.4,0.));
#8905=CARTESIAN_POINT('Origin',(0.,0.375,0.));
#8906=CARTESIAN_POINT('',(-0.35,0.35,-4.28626379701573E-17));
#8907=CARTESIAN_POINT('Origin',(0.,0.35,0.));
#8908=CARTESIAN_POINT('',(-0.325,0.375,-3.9801020972289E-17));
#8909=CARTESIAN_POINT('Origin',(0.,0.19,0.));
#8910=CARTESIAN_POINT('',(-0.35,0.03,-4.28626379701574E-17));
#8911=CARTESIAN_POINT('Origin',(0.,0.03,0.));
#8912=CARTESIAN_POINT('',(-0.35,0.19,-4.28626379701574E-17));
#8913=CARTESIAN_POINT('Origin',(0.,0.0149999999999999,0.));
#8914=CARTESIAN_POINT('',(-0.32,-3.29597460435593E-17,-3.91886975727153E-17));
#8915=CARTESIAN_POINT('Origin',(0.,0.,0.));
#8916=CARTESIAN_POINT('',(-0.335,0.0149999999999999,-4.10256677714363E-17));
#8917=CARTESIAN_POINT('Origin',(0.22,0.,0.));
#8918=CARTESIAN_POINT('',(-0.22,-6.93889390390723E-18,-2.69422295812418E-17));
#8919=CARTESIAN_POINT('Origin',(0.,0.,0.));
#8920=CARTESIAN_POINT('Origin',(0.,-0.02,0.));
#8921=CARTESIAN_POINT('',(-0.1954,-0.0492,2.39295984553393E-17));
#8922=CARTESIAN_POINT('Origin',(0.,-0.0492,0.));
#8923=CARTESIAN_POINT('',(-0.21,-0.02,-2.57175827820944E-17));
#8924=CARTESIAN_POINT('Origin',(0.,-0.8,0.));
#8925=CARTESIAN_POINT('',(-0.1954,-0.8,-2.39295984553393E-17));
#11217=UNCERTAINTY_MEASURE_WITH_UNIT(LENGTH_MEASURE(0.001),#11259,
'DISTANCE_ACCURACY_VALUE',
'Maximum model space distance between geometric entities at asserted c
onnectivities');
#11228=UNCERTAINTY_MEASURE_WITH_UNIT(LENGTH_MEASURE(0.001),#11259,
'DISTANCE_ACCURACY_VALUE',
'Maximum model space distance between geometric entities at asserted c
onnectivities');
#11247=(
GEOMETRIC_REPRESENTATION_CONTEXT(3)
GLOBAL_UNCERTAINTY_ASSIGNED_CONTEXT((#11217))
GLOBAL_UNIT_ASSIGNED_CONTEXT((#11259,#11261,#11262))
REPRESENTATION_CONTEXT('','3D')
);
#11258=(
GEOMETRIC_REPRESENTATION_CONTEXT(3)
GLOBAL_UNCERTAINTY_ASSIGNED_CONTEXT((#11228))
GLOBAL_UNIT_ASSIGNED_CONTEXT((#11259,#11261,#11262))
REPRESENTATION_CONTEXT('','3D')
);
#11259=(
LENGTH_UNIT()
NAMED_UNIT(*)
SI_UNIT(.CENTI.,.METRE.)
);
#11261=(
NAMED_UNIT(*)
PLANE_ANGLE_UNIT()
SI_UNIT($,.RADIAN.)
);
#11262=(
NAMED_UNIT(*)
SI_UNIT($,.STERADIAN.)
SOLID_ANGLE_UNIT()
);
#11281=SHAPE_DEFINITION_REPRESENTATION(#11315,#11377);
#11315=PRODUCT_DEFINITION_SHAPE('',$,#11407);
#11377=SHAPE_REPRESENTATION('',(#5838),#11247);
#11388=PRODUCT_DEFINITION_CONTEXT('part definition',#11477,'design');
#11407=PRODUCT_DEFINITION('M4x10 Cap Screw','M4x10 Cap Screw',#11436,#11388);
#11436=PRODUCT_DEFINITION_FORMATION('',$,#11497);
#11477=APPLICATION_CONTEXT(
'Core Data for Automotive Mechanical Design Process');
#11478=PRODUCT_CONTEXT('part definition',#11477,'mechanical');
#11497=PRODUCT('M4x10 Cap Screw','M4x10 Cap Screw','M4x10 Cap Screw',(#11478));
#11585=COLOUR_RGB('Black',0.12,0.14,0.17);
#11586=FILL_AREA_STYLE_COLOUR('',#11585);
#11587=FILL_AREA_STYLE('',(#11586));
#11588=SURFACE_STYLE_FILL_AREA(#11587);
#11589=SURFACE_SIDE_STYLE('',(#11588));
#11590=SURFACE_STYLE_USAGE(.BOTH.,#11589);
#11591=PRESENTATION_STYLE_ASSIGNMENT((#11590));
ENDSEC;
END-ISO-10303-21;
